ISO-10303-21;
HEADER;
/* Generated by software containing ST-Developer
 * from STEP Tools, Inc. (www.steptools.com) 
 */

FILE_DESCRIPTION(
/* description */ ('Cam-driven reciprocating slide'),
/* implementation_level */ '2;1');

FILE_NAME(
/* name */ 'Inner race sleeve 10 mm (1).step',
/* time_stamp */ '2026-10-28T03:25:20-07:00',
/* author */ (''),
/* organization */ (''),
/* preprocessor_version */ 'ST-DEVELOPER v20.2',
/* originating_system */ 'Autodesk Translation Framework v15.17.0.0',
/* authorisation */ '');

FILE_SCHEMA (('AUTOMOTIVE_DESIGN { 1 0 10303 214 3 1 1 }'));
ENDSEC;

DATA;
#10=MECHANICAL_DESIGN_GEOMETRIC_PRESENTATION_REPRESENTATION('',(#453),#13277);
#372=SHAPE_REPRESENTATION_RELATIONSHIP('SRR','None',#13468,#409);
#409=ADVANCED_BREP_SHAPE_REPRESENTATION('',(#495),#13263);
#453=STYLED_ITEM('',(#13720),#495);
#495=MANIFOLD_SOLID_BREP('Body1',#6431);
#646=FACE_BOUND('',#1700,.T.);
#647=FACE_BOUND('',#1702,.T.);
#835=PLANE('',#7429);
#836=PLANE('',#7430);
#1179=FACE_OUTER_BOUND('',#1697,.T.);
#1180=FACE_OUTER_BOUND('',#1698,.T.);
#1181=FACE_OUTER_BOUND('',#1699,.T.);
#1182=FACE_OUTER_BOUND('',#1701,.T.);
#1697=EDGE_LOOP('',(#5504,#5505,#5506,#5507));
#1698=EDGE_LOOP('',(#5508,#5509,#5510,#5511));
#1699=EDGE_LOOP('',(#5512));
#1700=EDGE_LOOP('',(#5513));
#1701=EDGE_LOOP('',(#5514));
#1702=EDGE_LOOP('',(#5515));
#2146=LINE('',#12694,#2585);
#2147=LINE('',#12700,#2586);
#2585=VECTOR('',#9126,0.605);
#2586=VECTOR('',#9133,0.8);
#2967=CIRCLE('',#7424,0.605);
#2968=CIRCLE('',#7425,0.605);
#2969=CIRCLE('',#7427,0.8);
#2970=CIRCLE('',#7428,0.8);
#3430=VERTEX_POINT('',#12691);
#3431=VERTEX_POINT('',#12693);
#3432=VERTEX_POINT('',#12697);
#3433=VERTEX_POINT('',#12699);
#4142=EDGE_CURVE('',#3430,#3430,#2967,.T.);
#4143=EDGE_CURVE('',#3430,#3431,#2146,.T.);
#4144=EDGE_CURVE('',#3431,#3431,#2968,.T.);
#4145=EDGE_CURVE('',#3432,#3432,#2969,.T.);
#4146=EDGE_CURVE('',#3432,#3433,#2147,.T.);
#4147=EDGE_CURVE('',#3433,#3433,#2970,.T.);
#5504=ORIENTED_EDGE('',*,*,#4142,.F.);
#5505=ORIENTED_EDGE('',*,*,#4143,.T.);
#5506=ORIENTED_EDGE('',*,*,#4144,.T.);
#5507=ORIENTED_EDGE('',*,*,#4143,.F.);
#5508=ORIENTED_EDGE('',*,*,#4145,.F.);
#5509=ORIENTED_EDGE('',*,*,#4146,.T.);
#5510=ORIENTED_EDGE('',*,*,#4147,.T.);
#5511=ORIENTED_EDGE('',*,*,#4146,.F.);
#5512=ORIENTED_EDGE('',*,*,#4145,.T.);
#5513=ORIENTED_EDGE('',*,*,#4142,.T.);
#5514=ORIENTED_EDGE('',*,*,#4147,.F.);
#5515=ORIENTED_EDGE('',*,*,#4144,.F.);
#5988=CYLINDRICAL_SURFACE('',#7423,0.605);
#5989=CYLINDRICAL_SURFACE('',#7426,0.8);
#6297=ADVANCED_FACE('',(#1179),#5988,.F.);
#6298=ADVANCED_FACE('',(#1180),#5989,.T.);
#6299=ADVANCED_FACE('',(#1181,#646),#835,.T.);
#6300=ADVANCED_FACE('',(#1182,#647),#836,.F.);
#6431=CLOSED_SHELL('',(#6297,#6298,#6299,#6300));
#7422=AXIS2_PLACEMENT_3D('',#12689,#9120,#9121);
#7423=AXIS2_PLACEMENT_3D('',#12690,#9122,#9123);
#7424=AXIS2_PLACEMENT_3D('',#12692,#9124,#9125);
#7425=AXIS2_PLACEMENT_3D('',#12695,#9127,#9128);
#7426=AXIS2_PLACEMENT_3D('',#12696,#9129,#9130);
#7427=AXIS2_PLACEMENT_3D('',#12698,#9131,#9132);
#7428=AXIS2_PLACEMENT_3D('',#12701,#9134,#9135);
#7429=AXIS2_PLACEMENT_3D('',#12702,#9136,#9137);
#7430=AXIS2_PLACEMENT_3D('',#12703,#9138,#9139);
#9120=DIRECTION('axis',(0.,0.,1.));
#9121=DIRECTION('refdir',(1.,0.,0.));
#9122=DIRECTION('center_axis',(0.,1.,0.));
#9123=DIRECTION('ref_axis',(1.,0.,0.));
#9124=DIRECTION('center_axis',(0.,-1.,0.));
#9125=DIRECTION('ref_axis',(1.,0.,0.));
#9126=DIRECTION('',(0.,-1.,0.));
#9127=DIRECTION('center_axis',(0.,-1.,0.));
#9128=DIRECTION('ref_axis',(1.,0.,0.));
#9129=DIRECTION('center_axis',(0.,1.,0.));
#9130=DIRECTION('ref_axis',(1.,0.,0.));
#9131=DIRECTION('center_axis',(0.,1.,0.));
#9132=DIRECTION('ref_axis',(1.,0.,0.));
#9133=DIRECTION('',(0.,-1.,0.));
#9134=DIRECTION('center_axis',(0.,1.,0.));
#9135=DIRECTION('ref_axis',(1.,0.,0.));
#9136=DIRECTION('center_axis',(0.,1.,0.));
#9137=DIRECTION('ref_axis',(1.,0.,0.));
#9138=DIRECTION('center_axis',(0.,1.,0.));
#9139=DIRECTION('ref_axis',(1.,0.,0.));
#12689=CARTESIAN_POINT('',(0.,0.,0.));
#12690=CARTESIAN_POINT('Origin',(0.,1.,4.));
#12691=CARTESIAN_POINT('',(-0.605,2.,4.));
#12692=CARTESIAN_POINT('Origin',(0.,2.,4.));
#12693=CARTESIAN_POINT('',(-0.605,1.,4.));
#12694=CARTESIAN_POINT('',(-0.605,1.,4.));
#12695=CARTESIAN_POINT('Origin',(0.,1.,4.));
#12696=CARTESIAN_POINT('Origin',(0.,1.,4.));
#12697=CARTESIAN_POINT('',(-0.8,2.,4.));
#12698=CARTESIAN_POINT('Origin',(0.,2.,4.));
#12699=CARTESIAN_POINT('',(-0.8,1.,4.));
#12700=CARTESIAN_POINT('',(-0.8,1.,4.));
#12701=CARTESIAN_POINT('Origin',(0.,1.,4.));
#12702=CARTESIAN_POINT('Origin',(0.,2.,4.));
#12703=CARTESIAN_POINT('Origin',(0.,1.,4.));
#13219=UNCERTAINTY_MEASURE_WITH_UNIT(LENGTH_MEASURE(0.001),#13278,
'DISTANCE_ACCURACY_VALUE',
'Maximum model space distance between geometric entities at asserted c
onnectivities');
#13233=UNCERTAINTY_MEASURE_WITH_UNIT(LENGTH_MEASURE(0.001),#13278,
'DISTANCE_ACCURACY_VALUE',
'Maximum model space distance between geometric entities at asserted c
onnectivities');
#13263=(
GEOMETRIC_REPRESENTATION_CONTEXT(3)
GLOBAL_UNCERTAINTY_ASSIGNED_CONTEXT((#13219))
GLOBAL_UNIT_ASSIGNED_CONTEXT((#13278,#13280,#13281))
REPRESENTATION_CONTEXT('','3D')
);
#13277=(
GEOMETRIC_REPRESENTATION_CONTEXT(3)
GLOBAL_UNCERTAINTY_ASSIGNED_CONTEXT((#13233))
GLOBAL_UNIT_ASSIGNED_CONTEXT((#13278,#13280,#13281))
REPRESENTATION_CONTEXT('','3D')
);
#13278=(
LENGTH_UNIT()
NAMED_UNIT(*)
SI_UNIT(.CENTI.,.METRE.)
);
#13280=(
NAMED_UNIT(*)
PLANE_ANGLE_UNIT()
SI_UNIT($,.RADIAN.)
);
#13281=(
NAMED_UNIT(*)
SI_UNIT($,.STERADIAN.)
SOLID_ANGLE_UNIT()
);
#13311=SHAPE_DEFINITION_REPRESENTATION(#13361,#13468);
#13361=PRODUCT_DEFINITION_SHAPE('',$,#13512);
#13468=SHAPE_REPRESENTATION('',(#7422),#13263);
#13482=PRODUCT_DEFINITION_CONTEXT('part definition',#13613,'design');
#13512=PRODUCT_DEFINITION('Inner race sleeve 10 mm (1)',
'Inner race sleeve 10 mm (1)',#13555,#13482);
#13555=PRODUCT_DEFINITION_FORMATION('',$,#13644);
#13613=APPLICATION_CONTEXT(
'Core Data for Automotive Mechanical Design Process');
#13614=PRODUCT_CONTEXT('part definition',#13613,'mechanical');
#13644=PRODUCT('Inner race sleeve 10 mm (1)',
'Inner race sleeve 10 mm (1)','Inner race sleeve 10 mm (1)',(#13614));
#13714=COLOUR_RGB('Grey',0.48,0.52,0.57);
#13715=FILL_AREA_STYLE_COLOUR('',#13714);
#13716=FILL_AREA_STYLE('',(#13715));
#13717=SURFACE_STYLE_FILL_AREA(#13716);
#13718=SURFACE_SIDE_STYLE('',(#13717));
#13719=SURFACE_STYLE_USAGE(.BOTH.,#13718);
#13720=PRESENTATION_STYLE_ASSIGNMENT((#13719));
ENDSEC;
END-ISO-10303-21;
